ISO-10303-21;
HEADER;
/* Generated by software containing ST-Developer
 * from STEP Tools, Inc. (www.steptools.com) 
 */

FILE_DESCRIPTION(
/* description */ ('STEP AP214'),
/* implementation_level */ '2;1');

FILE_NAME(
/* name */ 'Socket Head Cap Screw M10 x 1.5 x 130.step',
/* time_stamp */ '2026-11-14T06:43:04-08:00',
/* author */ (''),
/* organization */ (''),
/* preprocessor_version */ 'ST-DEVELOPER v20.2',
/* originating_system */ 'Autodesk Translation Framework v15.17.0.0',
/* authorisation */ '');

FILE_SCHEMA (('AUTOMOTIVE_DESIGN { 1 0 10303 214 3 1 1 }'));
ENDSEC;

DATA;
#10=MECHANICAL_DESIGN_GEOMETRIC_PRESENTATION_REPRESENTATION('',(#206),#5658);
#111=CONICAL_SURFACE('',#3457,4.0575,1.04719755119659);
#112=CONICAL_SURFACE('',#3469,7.,0.785398163397448);
#113=CONICAL_SURFACE('',#3477,4.172,0.785398163397561);
#174=TOROIDAL_SURFACE('',#3464,5.40000000000003,0.4);
#184=SHAPE_REPRESENTATION_RELATIONSHIP('SRR','None',#5714,#195);
#195=ADVANCED_BREP_SHAPE_REPRESENTATION('',(#217),#5655);
#206=STYLED_ITEM('',(#5770),#217);
#217=MANIFOLD_SOLID_BREP('Body1',#3068);
#265=CYLINDRICAL_SURFACE('',#3473,8.);
#266=CYLINDRICAL_SURFACE('',#3475,5.00000000000003);
#331=FACE_BOUND('',#722,.T.);
#332=FACE_BOUND('',#725,.T.);
#473=FACE_OUTER_BOUND('',#715,.T.);
#474=FACE_OUTER_BOUND('',#716,.T.);
#475=FACE_OUTER_BOUND('',#717,.T.);
#476=FACE_OUTER_BOUND('',#718,.T.);
#477=FACE_OUTER_BOUND('',#719,.T.);
#478=FACE_OUTER_BOUND('',#720,.T.);
#479=FACE_OUTER_BOUND('',#721,.T.);
#480=FACE_OUTER_BOUND('',#723,.T.);
#481=FACE_OUTER_BOUND('',#724,.T.);
#482=FACE_OUTER_BOUND('',#726,.T.);
#483=FACE_OUTER_BOUND('',#727,.T.);
#484=FACE_OUTER_BOUND('',#728,.T.);
#485=FACE_OUTER_BOUND('',#729,.T.);
#486=FACE_OUTER_BOUND('',#730,.T.);
#487=FACE_OUTER_BOUND('',#731,.T.);
#488=FACE_OUTER_BOUND('',#732,.T.);
#489=FACE_OUTER_BOUND('',#733,.T.);
#490=FACE_OUTER_BOUND('',#734,.T.);
#491=FACE_OUTER_BOUND('',#735,.T.);
#492=FACE_OUTER_BOUND('',#736,.T.);
#493=FACE_OUTER_BOUND('',#737,.T.);
#715=EDGE_LOOP('',(#2594,#2595,#2596,#2597,#2598,#2599,#2600,#2601));
#716=EDGE_LOOP('',(#2602,#2603,#2604,#2605,#2606));
#717=EDGE_LOOP('',(#2607,#2608,#2609,#2610,#2611));
#718=EDGE_LOOP('',(#2612,#2613,#2614,#2615,#2616));
#719=EDGE_LOOP('',(#2617,#2618,#2619,#2620,#2621));
#720=EDGE_LOOP('',(#2622,#2623,#2624,#2625));
#721=EDGE_LOOP('',(#2626));
#722=EDGE_LOOP('',(#2627,#2628,#2629,#2630,#2631,#2632));
#723=EDGE_LOOP('',(#2633));
#724=EDGE_LOOP('',(#2634));
#725=EDGE_LOOP('',(#2635));
#726=EDGE_LOOP('',(#2636,#2637,#2638,#2639,#2640));
#727=EDGE_LOOP('',(#2641,#2642,#2643,#2644,#2645));
#728=EDGE_LOOP('',(#2646,#2647,#2648,#2649,#2650));
#729=EDGE_LOOP('',(#2651,#2652,#2653,#2654,#2655));
#730=EDGE_LOOP('',(#2656,#2657,#2658,#2659,#2660));
#731=EDGE_LOOP('',(#2661,#2662,#2663,#2664,#2665));
#732=EDGE_LOOP('',(#2666,#2667,#2668));
#733=EDGE_LOOP('',(#2669,#2670,#2671));
#734=EDGE_LOOP('',(#2672,#2673,#2674));
#735=EDGE_LOOP('',(#2675,#2676,#2677));
#736=EDGE_LOOP('',(#2678,#2679,#2680));
#737=EDGE_LOOP('',(#2681,#2682,#2683));
#903=LINE('',#5414,#1099);
#904=LINE('',#5439,#1100);
#905=LINE('',#5444,#1101);
#906=LINE('',#5448,#1102);
#907=LINE('',#5452,#1103);
#908=LINE('',#5457,#1104);
#909=LINE('',#5459,#1105);
#910=LINE('',#5461,#1106);
#911=LINE('',#5463,#1107);
#912=LINE('',#5465,#1108);
#913=LINE('',#5466,#1109);
#914=LINE('',#5471,#1110);
#915=LINE('',#5472,#1111);
#916=LINE('',#5474,#1112);
#917=LINE('',#5475,#1113);
#918=LINE('',#5477,#1114);
#919=LINE('',#5479,#1115);
#920=LINE('',#5480,#1116);
#921=LINE('',#5482,#1117);
#922=LINE('',#5484,#1118);
#923=LINE('',#5485,#1119);
#924=LINE('',#5487,#1120);
#925=LINE('',#5489,#1121);
#926=LINE('',#5490,#1122);
#927=LINE('',#5492,#1123);
#928=LINE('',#5494,#1124);
#929=LINE('',#5495,#1125);
#930=LINE('',#5497,#1126);
#931=LINE('',#5498,#1127);
#1099=VECTOR('',#4225,4.0575);
#1100=VECTOR('',#4252,7.);
#1101=VECTOR('',#4259,8.);
#1102=VECTOR('',#4264,5.00000000000003);
#1103=VECTOR('',#4269,4.172);
#1104=VECTOR('',#4274,1000.);
#1105=VECTOR('',#4275,1000.);
#1106=VECTOR('',#4276,1000.);
#1107=VECTOR('',#4277,1000.);
#1108=VECTOR('',#4278,1000.);
#1109=VECTOR('',#4279,1000.);
#1110=VECTOR('',#4286,1000.);
#1111=VECTOR('',#4287,1000.);
#1112=VECTOR('',#4288,1000.);
#1113=VECTOR('',#4289,1000.);
#1114=VECTOR('',#4292,1000.);
#1115=VECTOR('',#4293,1000.);
#1116=VECTOR('',#4294,1000.);
#1117=VECTOR('',#4297,1000.);
#1118=VECTOR('',#4298,1000.);
#1119=VECTOR('',#4299,1000.);
#1120=VECTOR('',#4302,1000.);
#1121=VECTOR('',#4303,1000.);
#1122=VECTOR('',#4304,1000.);
#1123=VECTOR('',#4307,1000.);
#1124=VECTOR('',#4308,1000.);
#1125=VECTOR('',#4309,1000.);
#1126=VECTOR('',#4312,1000.);
#1127=VECTOR('',#4313,1000.);
#1278=CIRCLE('',#3458,4.0575);
#1279=CIRCLE('',#3459,4.0575);
#1280=CIRCLE('',#3460,4.0575);
#1281=CIRCLE('',#3461,4.0575);
#1282=CIRCLE('',#3462,4.0575);
#1283=CIRCLE('',#3463,4.0575);
#1284=CIRCLE('',#3465,5.00000000000003);
#1285=CIRCLE('',#3466,5.00000000000003);
#1286=CIRCLE('',#3467,0.4);
#1287=CIRCLE('',#3468,5.40000000000003);
#1288=CIRCLE('',#3470,8.);
#1289=CIRCLE('',#3471,7.);
#1290=CIRCLE('',#3472,8.);
#1291=CIRCLE('',#3474,8.);
#1292=CIRCLE('',#3476,5.00000000000007);
#1293=CIRCLE('',#3478,4.172);
#1511=VERTEX_POINT('',#5412);
#1512=VERTEX_POINT('',#5413);
#1513=VERTEX_POINT('',#5415);
#1514=VERTEX_POINT('',#5417);
#1515=VERTEX_POINT('',#5419);
#1516=VERTEX_POINT('',#5421);
#1517=VERTEX_POINT('',#5423);
#1518=VERTEX_POINT('',#5427);
#1519=VERTEX_POINT('',#5428);
#1520=VERTEX_POINT('',#5431);
#1521=VERTEX_POINT('',#5435);
#1522=VERTEX_POINT('',#5436);
#1523=VERTEX_POINT('',#5438);
#1524=VERTEX_POINT('',#5443);
#1525=VERTEX_POINT('',#5447);
#1526=VERTEX_POINT('',#5451);
#1527=VERTEX_POINT('',#5455);
#1528=VERTEX_POINT('',#5456);
#1529=VERTEX_POINT('',#5458);
#1530=VERTEX_POINT('',#5460);
#1531=VERTEX_POINT('',#5462);
#1532=VERTEX_POINT('',#5464);
#1533=VERTEX_POINT('',#5470);
#1534=VERTEX_POINT('',#5473);
#1535=VERTEX_POINT('',#5478);
#1536=VERTEX_POINT('',#5483);
#1537=VERTEX_POINT('',#5488);
#1538=VERTEX_POINT('',#5493);
#1880=EDGE_CURVE('',#1511,#1512,#903,.T.);
#1881=EDGE_CURVE('',#1512,#1513,#1278,.T.);
#1882=EDGE_CURVE('',#1513,#1514,#1279,.T.);
#1883=EDGE_CURVE('',#1514,#1515,#1280,.T.);
#1884=EDGE_CURVE('',#1515,#1516,#1281,.T.);
#1885=EDGE_CURVE('',#1516,#1517,#1282,.T.);
#1886=EDGE_CURVE('',#1517,#1512,#1283,.T.);
#1887=EDGE_CURVE('',#1518,#1519,#1284,.T.);
#1888=EDGE_CURVE('',#1519,#1518,#1285,.T.);
#1889=EDGE_CURVE('',#1519,#1520,#1286,.T.);
#1890=EDGE_CURVE('',#1520,#1520,#1287,.T.);
#1891=EDGE_CURVE('',#1521,#1522,#1288,.T.);
#1892=EDGE_CURVE('',#1522,#1523,#904,.T.);
#1893=EDGE_CURVE('',#1523,#1523,#1289,.T.);
#1894=EDGE_CURVE('',#1522,#1521,#1290,.T.);
#1895=EDGE_CURVE('',#1521,#1524,#905,.T.);
#1896=EDGE_CURVE('',#1524,#1524,#1291,.T.);
#1897=EDGE_CURVE('',#1518,#1525,#906,.T.);
#1898=EDGE_CURVE('',#1525,#1525,#1292,.T.);
#1899=EDGE_CURVE('',#1525,#1526,#907,.T.);
#1900=EDGE_CURVE('',#1526,#1526,#1293,.T.);
#1901=EDGE_CURVE('',#1527,#1528,#908,.T.);
#1902=EDGE_CURVE('',#1529,#1528,#909,.T.);
#1903=EDGE_CURVE('',#1529,#1530,#910,.T.);
#1904=EDGE_CURVE('',#1530,#1531,#911,.T.);
#1905=EDGE_CURVE('',#1532,#1531,#912,.T.);
#1906=EDGE_CURVE('',#1527,#1532,#913,.T.);
#1907=EDGE_CURVE('',#1533,#1527,#914,.T.);
#1908=EDGE_CURVE('',#1533,#1516,#915,.T.);
#1909=EDGE_CURVE('',#1516,#1534,#916,.T.);
#1910=EDGE_CURVE('',#1534,#1528,#917,.T.);
#1911=EDGE_CURVE('',#1515,#1534,#918,.T.);
#1912=EDGE_CURVE('',#1535,#1515,#919,.T.);
#1913=EDGE_CURVE('',#1535,#1529,#920,.T.);
#1914=EDGE_CURVE('',#1535,#1514,#921,.T.);
#1915=EDGE_CURVE('',#1514,#1536,#922,.T.);
#1916=EDGE_CURVE('',#1536,#1530,#923,.T.);
#1917=EDGE_CURVE('',#1536,#1513,#924,.T.);
#1918=EDGE_CURVE('',#1513,#1537,#925,.T.);
#1919=EDGE_CURVE('',#1537,#1531,#926,.T.);
#1920=EDGE_CURVE('',#1512,#1537,#927,.T.);
#1921=EDGE_CURVE('',#1538,#1512,#928,.T.);
#1922=EDGE_CURVE('',#1538,#1532,#929,.T.);
#1923=EDGE_CURVE('',#1517,#1538,#930,.T.);
#1924=EDGE_CURVE('',#1533,#1517,#931,.T.);
#2594=ORIENTED_EDGE('',*,*,#1880,.T.);
#2595=ORIENTED_EDGE('',*,*,#1881,.T.);
#2596=ORIENTED_EDGE('',*,*,#1882,.T.);
#2597=ORIENTED_EDGE('',*,*,#1883,.T.);
#2598=ORIENTED_EDGE('',*,*,#1884,.T.);
#2599=ORIENTED_EDGE('',*,*,#1885,.T.);
#2600=ORIENTED_EDGE('',*,*,#1886,.T.);
#2601=ORIENTED_EDGE('',*,*,#1880,.F.);
#2602=ORIENTED_EDGE('',*,*,#1887,.F.);
#2603=ORIENTED_EDGE('',*,*,#1888,.F.);
#2604=ORIENTED_EDGE('',*,*,#1889,.T.);
#2605=ORIENTED_EDGE('',*,*,#1890,.F.);
#2606=ORIENTED_EDGE('',*,*,#1889,.F.);
#2607=ORIENTED_EDGE('',*,*,#1891,.T.);
#2608=ORIENTED_EDGE('',*,*,#1892,.T.);
#2609=ORIENTED_EDGE('',*,*,#1893,.F.);
#2610=ORIENTED_EDGE('',*,*,#1892,.F.);
#2611=ORIENTED_EDGE('',*,*,#1894,.T.);
#2612=ORIENTED_EDGE('',*,*,#1891,.F.);
#2613=ORIENTED_EDGE('',*,*,#1895,.T.);
#2614=ORIENTED_EDGE('',*,*,#1896,.T.);
#2615=ORIENTED_EDGE('',*,*,#1895,.F.);
#2616=ORIENTED_EDGE('',*,*,#1894,.F.);
#2617=ORIENTED_EDGE('',*,*,#1887,.T.);
#2618=ORIENTED_EDGE('',*,*,#1888,.T.);
#2619=ORIENTED_EDGE('',*,*,#1897,.T.);
#2620=ORIENTED_EDGE('',*,*,#1898,.T.);
#2621=ORIENTED_EDGE('',*,*,#1897,.F.);
#2622=ORIENTED_EDGE('',*,*,#1898,.F.);
#2623=ORIENTED_EDGE('',*,*,#1899,.T.);
#2624=ORIENTED_EDGE('',*,*,#1900,.T.);
#2625=ORIENTED_EDGE('',*,*,#1899,.F.);
#2626=ORIENTED_EDGE('',*,*,#1893,.T.);
#2627=ORIENTED_EDGE('',*,*,#1901,.T.);
#2628=ORIENTED_EDGE('',*,*,#1902,.F.);
#2629=ORIENTED_EDGE('',*,*,#1903,.T.);
#2630=ORIENTED_EDGE('',*,*,#1904,.T.);
#2631=ORIENTED_EDGE('',*,*,#1905,.F.);
#2632=ORIENTED_EDGE('',*,*,#1906,.F.);
#2633=ORIENTED_EDGE('',*,*,#1900,.F.);
#2634=ORIENTED_EDGE('',*,*,#1896,.F.);
#2635=ORIENTED_EDGE('',*,*,#1890,.T.);
#2636=ORIENTED_EDGE('',*,*,#1901,.F.);
#2637=ORIENTED_EDGE('',*,*,#1907,.F.);
#2638=ORIENTED_EDGE('',*,*,#1908,.T.);
#2639=ORIENTED_EDGE('',*,*,#1909,.T.);
#2640=ORIENTED_EDGE('',*,*,#1910,.T.);
#2641=ORIENTED_EDGE('',*,*,#1902,.T.);
#2642=ORIENTED_EDGE('',*,*,#1910,.F.);
#2643=ORIENTED_EDGE('',*,*,#1911,.F.);
#2644=ORIENTED_EDGE('',*,*,#1912,.F.);
#2645=ORIENTED_EDGE('',*,*,#1913,.T.);
#2646=ORIENTED_EDGE('',*,*,#1903,.F.);
#2647=ORIENTED_EDGE('',*,*,#1913,.F.);
#2648=ORIENTED_EDGE('',*,*,#1914,.T.);
#2649=ORIENTED_EDGE('',*,*,#1915,.T.);
#2650=ORIENTED_EDGE('',*,*,#1916,.T.);
#2651=ORIENTED_EDGE('',*,*,#1904,.F.);
#2652=ORIENTED_EDGE('',*,*,#1916,.F.);
#2653=ORIENTED_EDGE('',*,*,#1917,.T.);
#2654=ORIENTED_EDGE('',*,*,#1918,.T.);
#2655=ORIENTED_EDGE('',*,*,#1919,.T.);
#2656=ORIENTED_EDGE('',*,*,#1905,.T.);
#2657=ORIENTED_EDGE('',*,*,#1919,.F.);
#2658=ORIENTED_EDGE('',*,*,#1920,.F.);
#2659=ORIENTED_EDGE('',*,*,#1921,.F.);
#2660=ORIENTED_EDGE('',*,*,#1922,.T.);
#2661=ORIENTED_EDGE('',*,*,#1906,.T.);
#2662=ORIENTED_EDGE('',*,*,#1922,.F.);
#2663=ORIENTED_EDGE('',*,*,#1923,.F.);
#2664=ORIENTED_EDGE('',*,*,#1924,.F.);
#2665=ORIENTED_EDGE('',*,*,#1907,.T.);
#2666=ORIENTED_EDGE('',*,*,#1920,.T.);
#2667=ORIENTED_EDGE('',*,*,#1918,.F.);
#2668=ORIENTED_EDGE('',*,*,#1881,.F.);
#2669=ORIENTED_EDGE('',*,*,#1917,.F.);
#2670=ORIENTED_EDGE('',*,*,#1915,.F.);
#2671=ORIENTED_EDGE('',*,*,#1882,.F.);
#2672=ORIENTED_EDGE('',*,*,#1914,.F.);
#2673=ORIENTED_EDGE('',*,*,#1912,.T.);
#2674=ORIENTED_EDGE('',*,*,#1883,.F.);
#2675=ORIENTED_EDGE('',*,*,#1911,.T.);
#2676=ORIENTED_EDGE('',*,*,#1909,.F.);
#2677=ORIENTED_EDGE('',*,*,#1884,.F.);
#2678=ORIENTED_EDGE('',*,*,#1908,.F.);
#2679=ORIENTED_EDGE('',*,*,#1924,.T.);
#2680=ORIENTED_EDGE('',*,*,#1885,.F.);
#2681=ORIENTED_EDGE('',*,*,#1923,.T.);
#2682=ORIENTED_EDGE('',*,*,#1921,.T.);
#2683=ORIENTED_EDGE('',*,*,#1886,.F.);
#2846=PLANE('',#3479);
#2847=PLANE('',#3480);
#2848=PLANE('',#3481);
#2849=PLANE('',#3482);
#2850=PLANE('',#3483);
#2851=PLANE('',#3484);
#2852=PLANE('',#3485);
#2853=PLANE('',#3486);
#2854=PLANE('',#3487);
#2855=PLANE('',#3488);
#2856=PLANE('',#3489);
#2857=PLANE('',#3490);
#2858=PLANE('',#3491);
#2859=PLANE('',#3492);
#2860=PLANE('',#3493);
#3014=ADVANCED_FACE('',(#473),#111,.F.);
#3015=ADVANCED_FACE('',(#474),#174,.F.);
#3016=ADVANCED_FACE('',(#475),#112,.T.);
#3017=ADVANCED_FACE('',(#476),#265,.T.);
#3018=ADVANCED_FACE('',(#477),#266,.T.);
#3019=ADVANCED_FACE('',(#478),#113,.T.);
#3020=ADVANCED_FACE('',(#479,#331),#2846,.T.);
#3021=ADVANCED_FACE('',(#480),#2847,.T.);
#3022=ADVANCED_FACE('',(#481,#332),#2848,.T.);
#3023=ADVANCED_FACE('',(#482),#2849,.T.);
#3024=ADVANCED_FACE('',(#483),#2850,.F.);
#3025=ADVANCED_FACE('',(#484),#2851,.T.);
#3026=ADVANCED_FACE('',(#485),#2852,.T.);
#3027=ADVANCED_FACE('',(#486),#2853,.F.);
#3028=ADVANCED_FACE('',(#487),#2854,.F.);
#3029=ADVANCED_FACE('',(#488),#2855,.F.);
#3030=ADVANCED_FACE('',(#489),#2856,.F.);
#3031=ADVANCED_FACE('',(#490),#2857,.F.);
#3032=ADVANCED_FACE('',(#491),#2858,.F.);
#3033=ADVANCED_FACE('',(#492),#2859,.F.);
#3034=ADVANCED_FACE('',(#493),#2860,.F.);
#3068=CLOSED_SHELL('',(#3014,#3015,#3016,#3017,#3018,#3019,#3020,#3021,
#3022,#3023,#3024,#3025,#3026,#3027,#3028,#3029,#3030,#3031,#3032,#3033,
#3034));
#3456=AXIS2_PLACEMENT_3D('',#5410,#4221,#4222);
#3457=AXIS2_PLACEMENT_3D('',#5411,#4223,#4224);
#3458=AXIS2_PLACEMENT_3D('',#5416,#4226,#4227);
#3459=AXIS2_PLACEMENT_3D('',#5418,#4228,#4229);
#3460=AXIS2_PLACEMENT_3D('',#5420,#4230,#4231);
#3461=AXIS2_PLACEMENT_3D('',#5422,#4232,#4233);
#3462=AXIS2_PLACEMENT_3D('',#5424,#4234,#4235);
#3463=AXIS2_PLACEMENT_3D('',#5425,#4236,#4237);
#3464=AXIS2_PLACEMENT_3D('',#5426,#4238,#4239);
#3465=AXIS2_PLACEMENT_3D('',#5429,#4240,#4241);
#3466=AXIS2_PLACEMENT_3D('',#5430,#4242,#4243);
#3467=AXIS2_PLACEMENT_3D('',#5432,#4244,#4245);
#3468=AXIS2_PLACEMENT_3D('',#5433,#4246,#4247);
#3469=AXIS2_PLACEMENT_3D('',#5434,#4248,#4249);
#3470=AXIS2_PLACEMENT_3D('',#5437,#4250,#4251);
#3471=AXIS2_PLACEMENT_3D('',#5440,#4253,#4254);
#3472=AXIS2_PLACEMENT_3D('',#5441,#4255,#4256);
#3473=AXIS2_PLACEMENT_3D('',#5442,#4257,#4258);
#3474=AXIS2_PLACEMENT_3D('',#5445,#4260,#4261);
#3475=AXIS2_PLACEMENT_3D('',#5446,#4262,#4263);
#3476=AXIS2_PLACEMENT_3D('',#5449,#4265,#4266);
#3477=AXIS2_PLACEMENT_3D('',#5450,#4267,#4268);
#3478=AXIS2_PLACEMENT_3D('',#5453,#4270,#4271);
#3479=AXIS2_PLACEMENT_3D('',#5454,#4272,#4273);
#3480=AXIS2_PLACEMENT_3D('',#5467,#4280,#4281);
#3481=AXIS2_PLACEMENT_3D('',#5468,#4282,#4283);
#3482=AXIS2_PLACEMENT_3D('',#5469,#4284,#4285);
#3483=AXIS2_PLACEMENT_3D('',#5476,#4290,#4291);
#3484=AXIS2_PLACEMENT_3D('',#5481,#4295,#4296);
#3485=AXIS2_PLACEMENT_3D('',#5486,#4300,#4301);
#3486=AXIS2_PLACEMENT_3D('',#5491,#4305,#4306);
#3487=AXIS2_PLACEMENT_3D('',#5496,#4310,#4311);
#3488=AXIS2_PLACEMENT_3D('',#5499,#4314,#4315);
#3489=AXIS2_PLACEMENT_3D('',#5500,#4316,#4317);
#3490=AXIS2_PLACEMENT_3D('',#5501,#4318,#4319);
#3491=AXIS2_PLACEMENT_3D('',#5502,#4320,#4321);
#3492=AXIS2_PLACEMENT_3D('',#5503,#4322,#4323);
#3493=AXIS2_PLACEMENT_3D('',#5504,#4324,#4325);
#4221=DIRECTION('axis',(0.,0.,1.));
#4222=DIRECTION('refdir',(1.,0.,0.));
#4223=DIRECTION('center_axis',(-1.,0.,0.));
#4224=DIRECTION('ref_axis',(0.,0.,1.));
#4225=DIRECTION('',(-0.500000000000004,-1.0605752387249E-16,-0.866025403784436));
#4226=DIRECTION('center_axis',(-1.,0.,0.));
#4227=DIRECTION('ref_axis',(0.,0.,1.));
#4228=DIRECTION('center_axis',(-1.,0.,0.));
#4229=DIRECTION('ref_axis',(0.,0.,1.));
#4230=DIRECTION('center_axis',(-1.,0.,0.));
#4231=DIRECTION('ref_axis',(0.,0.,1.));
#4232=DIRECTION('center_axis',(-1.,0.,0.));
#4233=DIRECTION('ref_axis',(0.,0.,1.));
#4234=DIRECTION('center_axis',(-1.,0.,0.));
#4235=DIRECTION('ref_axis',(0.,0.,1.));
#4236=DIRECTION('center_axis',(-1.,0.,0.));
#4237=DIRECTION('ref_axis',(0.,0.,1.));
#4238=DIRECTION('center_axis',(1.,0.,0.));
#4239=DIRECTION('ref_axis',(0.,0.,-1.));
#4240=DIRECTION('center_axis',(1.,0.,0.));
#4241=DIRECTION('ref_axis',(0.,0.,-1.));
#4242=DIRECTION('center_axis',(1.,0.,0.));
#4243=DIRECTION('ref_axis',(0.,0.,-1.));
#4244=DIRECTION('center_axis',(0.,1.,1.22464679914735E-16));
#4245=DIRECTION('ref_axis',(0.,-1.22464679914735E-16,1.));
#4246=DIRECTION('center_axis',(-1.,0.,0.));
#4247=DIRECTION('ref_axis',(0.,0.,-1.));
#4248=DIRECTION('center_axis',(1.,0.,0.));
#4249=DIRECTION('ref_axis',(0.,0.,-1.));
#4250=DIRECTION('center_axis',(-1.,0.,0.));
#4251=DIRECTION('ref_axis',(0.,0.,1.));
#4252=DIRECTION('',(-0.707106781186548,8.65956056235493E-17,-0.707106781186548));
#4253=DIRECTION('center_axis',(-1.,0.,0.));
#4254=DIRECTION('ref_axis',(0.,0.,1.));
#4255=DIRECTION('center_axis',(-1.,0.,0.));
#4256=DIRECTION('ref_axis',(0.,0.,1.));
#4257=DIRECTION('center_axis',(-1.,0.,0.));
#4258=DIRECTION('ref_axis',(0.,0.,1.));
#4259=DIRECTION('',(1.,0.,0.));
#4260=DIRECTION('center_axis',(-1.,0.,0.));
#4261=DIRECTION('ref_axis',(0.,0.,1.));
#4262=DIRECTION('center_axis',(-1.,0.,0.));
#4263=DIRECTION('ref_axis',(0.,0.,1.));
#4264=DIRECTION('',(1.,0.,0.));
#4265=DIRECTION('center_axis',(-1.,0.,0.));
#4266=DIRECTION('ref_axis',(0.,0.,1.));
#4267=DIRECTION('center_axis',(-1.,0.,0.));
#4268=DIRECTION('ref_axis',(0.,0.,1.));
#4269=DIRECTION('',(0.707106781186468,8.6595605623559E-17,0.707106781186627));
#4270=DIRECTION('center_axis',(-1.,0.,0.));
#4271=DIRECTION('ref_axis',(0.,0.,1.));
#4272=DIRECTION('center_axis',(-1.,0.,0.));
#4273=DIRECTION('ref_axis',(0.,0.,1.));
#4274=DIRECTION('',(0.,-0.499999999999999,0.866025403784439));
#4275=DIRECTION('',(0.,1.,-1.11076864971324E-15));
#4276=DIRECTION('',(0.,-0.500000000000001,-0.866025403784438));
#4277=DIRECTION('',(0.,0.499999999999999,-0.866025403784439));
#4278=DIRECTION('',(0.,-1.,7.40512433142161E-16));
#4279=DIRECTION('',(0.,-0.500000000000001,-0.866025403784438));
#4280=DIRECTION('center_axis',(1.,0.,0.));
#4281=DIRECTION('ref_axis',(0.,0.,-1.));
#4282=DIRECTION('center_axis',(1.,0.,0.));
#4283=DIRECTION('ref_axis',(0.,0.,-1.));
#4284=DIRECTION('center_axis',(0.,-0.866025403784439,-0.499999999999999));
#4285=DIRECTION('ref_axis',(0.,0.499999999999999,-0.866025403784439));
#4286=DIRECTION('',(-1.,0.,0.));
#4287=DIRECTION('',(0.,-0.499999999999999,0.866025403784439));
#4288=DIRECTION('',(0.,-0.499999999999999,0.866025403784439));
#4289=DIRECTION('',(-1.,0.,0.));
#4290=DIRECTION('center_axis',(0.,1.11076864971324E-15,1.));
#4291=DIRECTION('ref_axis',(0.,-1.,1.11076864971324E-15));
#4292=DIRECTION('',(0.,1.,-1.11076864971324E-15));
#4293=DIRECTION('',(0.,1.,-1.11076864971324E-15));
#4294=DIRECTION('',(-1.,0.,0.));
#4295=DIRECTION('center_axis',(0.,0.866025403784438,-0.500000000000001));
#4296=DIRECTION('ref_axis',(0.,0.500000000000001,0.866025403784438));
#4297=DIRECTION('',(0.,-0.500000000000001,-0.866025403784438));
#4298=DIRECTION('',(0.,-0.500000000000001,-0.866025403784438));
#4299=DIRECTION('',(-1.,0.,0.));
#4300=DIRECTION('center_axis',(0.,0.866025403784439,0.499999999999999));
#4301=DIRECTION('ref_axis',(0.,-0.499999999999999,0.866025403784439));
#4302=DIRECTION('',(0.,0.499999999999999,-0.866025403784439));
#4303=DIRECTION('',(0.,0.499999999999999,-0.866025403784439));
#4304=DIRECTION('',(-1.,0.,0.));
#4305=DIRECTION('center_axis',(0.,-7.40512433142161E-16,-1.));
#4306=DIRECTION('ref_axis',(0.,1.,-7.40512433142161E-16));
#4307=DIRECTION('',(0.,-1.,7.40512433142161E-16));
#4308=DIRECTION('',(0.,-1.,7.40512433142161E-16));
#4309=DIRECTION('',(-1.,0.,0.));
#4310=DIRECTION('center_axis',(0.,0.866025403784438,-0.500000000000001));
#4311=DIRECTION('ref_axis',(0.,0.500000000000001,0.866025403784438));
#4312=DIRECTION('',(0.,-0.500000000000001,-0.866025403784438));
#4313=DIRECTION('',(0.,-0.500000000000001,-0.866025403784438));
#4314=DIRECTION('center_axis',(1.,0.,0.));
#4315=DIRECTION('ref_axis',(0.,0.,-1.));
#4316=DIRECTION('center_axis',(1.,0.,0.));
#4317=DIRECTION('ref_axis',(0.,0.,-1.));
#4318=DIRECTION('center_axis',(1.,0.,0.));
#4319=DIRECTION('ref_axis',(0.,0.,-1.));
#4320=DIRECTION('center_axis',(1.,0.,0.));
#4321=DIRECTION('ref_axis',(0.,0.,-1.));
#4322=DIRECTION('center_axis',(1.,0.,0.));
#4323=DIRECTION('ref_axis',(0.,0.,-1.));
#4324=DIRECTION('center_axis',(1.,0.,0.));
#4325=DIRECTION('ref_axis',(0.,0.,-1.));
#5410=CARTESIAN_POINT('',(0.,0.,0.));
#5411=CARTESIAN_POINT('Origin',(4.99999999999999,0.,0.));
#5412=CARTESIAN_POINT('',(7.34259871723693,0.,0.));
#5413=CARTESIAN_POINT('',(4.99999999999999,-3.00462919747432E-15,-4.0575));
#5414=CARTESIAN_POINT('',(4.99999999999999,-4.96900438754039E-16,-4.0575));
#5415=CARTESIAN_POINT('',(5.,-3.51389807585536,-2.02875));
#5416=CARTESIAN_POINT('Origin',(4.99999999999999,0.,0.));
#5417=CARTESIAN_POINT('',(5.,-3.51389807585536,2.02875));
#5418=CARTESIAN_POINT('Origin',(4.99999999999999,0.,0.));
#5419=CARTESIAN_POINT('',(5.,4.50694379621148E-15,4.0575));
#5420=CARTESIAN_POINT('Origin',(4.99999999999999,0.,0.));
#5421=CARTESIAN_POINT('',(5.,3.51389807585536,2.02875));
#5422=CARTESIAN_POINT('Origin',(4.99999999999999,0.,0.));
#5423=CARTESIAN_POINT('',(5.,3.51389807585536,-2.02875000000001));
#5424=CARTESIAN_POINT('Origin',(4.99999999999999,0.,0.));
#5425=CARTESIAN_POINT('Origin',(4.99999999999999,0.,0.));
#5426=CARTESIAN_POINT('Origin',(10.4,0.,0.));
#5427=CARTESIAN_POINT('',(10.4,6.12323399573681E-16,-5.00000000000003));
#5428=CARTESIAN_POINT('',(10.4,-6.12323399573681E-16,5.00000000000003));
#5429=CARTESIAN_POINT('Origin',(10.4,0.,0.));
#5430=CARTESIAN_POINT('Origin',(10.4,0.,0.));
#5431=CARTESIAN_POINT('',(9.99999999999999,-6.61309271539575E-16,5.40000000000003));
#5432=CARTESIAN_POINT('Origin',(10.4,-6.61309271539575E-16,5.40000000000003));
#5433=CARTESIAN_POINT('Origin',(9.99999999999999,0.,0.));
#5434=CARTESIAN_POINT('Origin',(0.,0.,0.));
#5435=CARTESIAN_POINT('',(1.,9.79717439317883E-16,-8.));
#5436=CARTESIAN_POINT('',(1.,-9.79717439317883E-16,8.));
#5437=CARTESIAN_POINT('Origin',(1.,0.,0.));
#5438=CARTESIAN_POINT('',(-2.69313897121051E-16,-8.57252759403147E-16,7.));
#5439=CARTESIAN_POINT('',(0.,-8.57252759403147E-16,7.));
#5440=CARTESIAN_POINT('Origin',(0.,0.,0.));
#5441=CARTESIAN_POINT('Origin',(1.,0.,0.));
#5442=CARTESIAN_POINT('Origin',(-31.75,0.,0.));
#5443=CARTESIAN_POINT('',(10.,-9.79717439317883E-16,-8.));
#5444=CARTESIAN_POINT('',(-31.75,-9.79717439317883E-16,-8.));
#5445=CARTESIAN_POINT('Origin',(10.,0.,0.));
#5446=CARTESIAN_POINT('Origin',(-31.75,0.,0.));
#5447=CARTESIAN_POINT('',(139.172,-6.12323399573681E-16,-5.00000000000003));
#5448=CARTESIAN_POINT('',(-31.75,-6.12323399573681E-16,-5.00000000000003));
#5449=CARTESIAN_POINT('Origin',(139.172,0.,0.));
#5450=CARTESIAN_POINT('Origin',(140.,0.,0.));
#5451=CARTESIAN_POINT('',(140.,-5.10922644604276E-16,-4.172));
#5452=CARTESIAN_POINT('',(140.,-5.10922644604276E-16,-4.172));
#5453=CARTESIAN_POINT('Origin',(140.,0.,0.));
#5454=CARTESIAN_POINT('Origin',(2.72783148596379E-17,0.,0.));
#5455=CARTESIAN_POINT('',(0.,4.68519743447381,-5.63785129692462E-15));
#5456=CARTESIAN_POINT('',(0.,2.34259871723691,4.0575));
#5457=CARTESIAN_POINT('',(0.,4.68519743447381,-5.63785129692462E-15));
#5458=CARTESIAN_POINT('',(0.,-2.3425987172369,4.0575));
#5459=CARTESIAN_POINT('',(0.,-2.3425987172369,4.0575));
#5460=CARTESIAN_POINT('',(0.,-4.68519743447381,5.63785129692462E-15));
#5461=CARTESIAN_POINT('',(0.,-2.3425987172369,4.0575));
#5462=CARTESIAN_POINT('',(0.,-2.34259871723691,-4.0575));
#5463=CARTESIAN_POINT('',(0.,-4.68519743447381,5.63785129692462E-15));
#5464=CARTESIAN_POINT('',(0.,2.3425987172369,-4.0575));
#5465=CARTESIAN_POINT('',(0.,2.3425987172369,-4.0575));
#5466=CARTESIAN_POINT('',(0.,4.68519743447381,-5.63785129692462E-15));
#5467=CARTESIAN_POINT('Origin',(140.,4.172,0.));
#5468=CARTESIAN_POINT('Origin',(9.99999999999999,8.,0.));
#5469=CARTESIAN_POINT('Origin',(5.,4.68519743447381,-5.63785129692462E-15));
#5470=CARTESIAN_POINT('',(5.,4.68519743447381,-5.63785129692462E-15));
#5471=CARTESIAN_POINT('',(5.,4.68519743447381,-5.63785129692462E-15));
#5472=CARTESIAN_POINT('',(5.,4.68519743447381,-5.63785129692462E-15));
#5473=CARTESIAN_POINT('',(5.,2.34259871723691,4.0575));
#5474=CARTESIAN_POINT('',(5.,4.68519743447381,-5.63785129692462E-15));
#5475=CARTESIAN_POINT('',(5.,2.34259871723691,4.0575));
#5476=CARTESIAN_POINT('Origin',(5.,-2.3425987172369,4.0575));
#5477=CARTESIAN_POINT('',(5.,-2.3425987172369,4.0575));
#5478=CARTESIAN_POINT('',(5.,-2.3425987172369,4.0575));
#5479=CARTESIAN_POINT('',(5.,-2.3425987172369,4.0575));
#5480=CARTESIAN_POINT('',(5.,-2.3425987172369,4.0575));
#5481=CARTESIAN_POINT('Origin',(5.,-2.3425987172369,4.0575));
#5482=CARTESIAN_POINT('',(5.,-2.3425987172369,4.0575));
#5483=CARTESIAN_POINT('',(5.,-4.68519743447381,5.63785129692462E-15));
#5484=CARTESIAN_POINT('',(5.,-2.3425987172369,4.0575));
#5485=CARTESIAN_POINT('',(5.,-4.68519743447381,5.63785129692462E-15));
#5486=CARTESIAN_POINT('Origin',(5.,-4.68519743447381,5.63785129692462E-15));
#5487=CARTESIAN_POINT('',(5.,-4.68519743447381,5.63785129692462E-15));
#5488=CARTESIAN_POINT('',(5.,-2.34259871723691,-4.0575));
#5489=CARTESIAN_POINT('',(5.,-4.68519743447381,5.63785129692462E-15));
#5490=CARTESIAN_POINT('',(5.,-2.34259871723691,-4.0575));
#5491=CARTESIAN_POINT('Origin',(5.,2.3425987172369,-4.0575));
#5492=CARTESIAN_POINT('',(5.,2.3425987172369,-4.0575));
#5493=CARTESIAN_POINT('',(5.,2.3425987172369,-4.0575));
#5494=CARTESIAN_POINT('',(5.,2.3425987172369,-4.0575));
#5495=CARTESIAN_POINT('',(5.,2.3425987172369,-4.0575));
#5496=CARTESIAN_POINT('Origin',(5.,4.68519743447381,-5.63785129692462E-15));
#5497=CARTESIAN_POINT('',(5.,4.68519743447381,-5.63785129692462E-15));
#5498=CARTESIAN_POINT('',(5.,4.68519743447381,-5.63785129692462E-15));
#5499=CARTESIAN_POINT('Origin',(5.,7.02779615171071,-4.05750000000001));
#5500=CARTESIAN_POINT('Origin',(5.,7.02779615171071,-4.05750000000001));
#5501=CARTESIAN_POINT('Origin',(5.,7.02779615171071,-4.05750000000001));
#5502=CARTESIAN_POINT('Origin',(5.,7.02779615171071,-4.05750000000001));
#5503=CARTESIAN_POINT('Origin',(5.,7.02779615171071,-4.05750000000001));
#5504=CARTESIAN_POINT('Origin',(5.,7.02779615171071,-4.05750000000001));
#5642=UNCERTAINTY_MEASURE_WITH_UNIT(LENGTH_MEASURE(0.01),#5659,
'DISTANCE_ACCURACY_VALUE',
'Maximum model space distance between geometric entities at asserted c
onnectivities');
#5645=UNCERTAINTY_MEASURE_WITH_UNIT(LENGTH_MEASURE(0.01),#5659,
'DISTANCE_ACCURACY_VALUE',
'Maximum model space distance between geometric entities at asserted c
onnectivities');
#5655=(
GEOMETRIC_REPRESENTATION_CONTEXT(3)
GLOBAL_UNCERTAINTY_ASSIGNED_CONTEXT((#5642))
GLOBAL_UNIT_ASSIGNED_CONTEXT((#5659,#5661,#5662))
REPRESENTATION_CONTEXT('','3D')
);
#5658=(
GEOMETRIC_REPRESENTATION_CONTEXT(3)
GLOBAL_UNCERTAINTY_ASSIGNED_CONTEXT((#5645))
GLOBAL_UNIT_ASSIGNED_CONTEXT((#5659,#5661,#5662))
REPRESENTATION_CONTEXT('','3D')
);
#5659=(
LENGTH_UNIT()
NAMED_UNIT(*)
SI_UNIT(.MILLI.,.METRE.)
);
#5661=(
NAMED_UNIT(*)
PLANE_ANGLE_UNIT()
SI_UNIT($,.RADIAN.)
);
#5662=(
NAMED_UNIT(*)
SI_UNIT($,.STERADIAN.)
SOLID_ANGLE_UNIT()
);
#5672=SHAPE_DEFINITION_REPRESENTATION(#5684,#5714);
#5684=PRODUCT_DEFINITION_SHAPE('',$,#5727);
#5714=SHAPE_REPRESENTATION('',(#3456),#5655);
#5717=PRODUCT_DEFINITION_CONTEXT('part definition',#5755,'design');
#5727=PRODUCT_DEFINITION('Socket Head Cap Screw M10 x 1.5 x 130',
'Socket Head Cap Screw M10 x 1.5 x 130',#5739,#5717);
#5739=PRODUCT_DEFINITION_FORMATION('',$,#5766);
#5755=APPLICATION_CONTEXT(
'Core Data for Automotive Mechanical Design Process');
#5756=PRODUCT_CONTEXT('part definition',#5755,'mechanical');
#5766=PRODUCT('Socket Head Cap Screw M10 x 1.5 x 130',
'Socket Head Cap Screw M10 x 1.5 x 130',$,(#5756));
#5770=PRESENTATION_STYLE_ASSIGNMENT((#5775));
#5775=SURFACE_STYLE_USAGE(.BOTH.,#5780);
#5780=SURFACE_SIDE_STYLE('',(#5785));
#5785=SURFACE_STYLE_FILL_AREA(#5790);
#5790=FILL_AREA_STYLE('Opaque(31,36,43)',(#5795));
#5795=FILL_AREA_STYLE_COLOUR('Opaque(31,36,43)',#5800);
#5800=COLOUR_RGB('Opaque(31,36,43)',0.12156862745098,0.141176470588235,
0.168627450980392);
ENDSEC;
END-ISO-10303-21;
